ISO-10303-21;
HEADER;
FILE_DESCRIPTION (('STEP AP203'),
    '1' );
FILE_NAME ('Cleco, Fastener, Pusher.step',
    '2026-10-09T13:45:32',
    ( '' ),
    ( '' ),
    'SwSTEP 2.0',
    'SolidWorks 2024',
    '' );
FILE_SCHEMA (( 'AUTOMOTIVE_DESIGN' ));
ENDSEC;

DATA;
#12=ORIENTED_EDGE ( 'NONE', *, *, #4444, .T. ) ;
#18=DIRECTION ( 'NONE',  ( 0.000000000000000000, 0.000000000000000000, -1.000000000000000000 ) ) ;
#29=EDGE_CURVE ( 'NONE', #3273, #1544, #5158, .T. ) ;
#49=AXIS2_PLACEMENT_3D ( 'NONE', #6623, #1014, #5431 ) ;
#92=AXIS2_PLACEMENT_3D ( 'NONE', #7571, #6383, #766 ) ;
#97=CARTESIAN_POINT ( 'NONE',  ( 0.000000000000000000, 0.03124999999999997571, 0.000000000000000000 ) ) ;
#99=ORIENTED_EDGE ( 'NONE', *, *, #6424, .F. ) ;
#131=EDGE_CURVE ( 'NONE', #668, #4233, #6788, .T. ) ;
#135=DIRECTION ( 'NONE',  ( 1.000000000000000000, 0.000000000000000000, 0.000000000000000000 ) ) ;
#168=EDGE_CURVE ( 'NONE', #5062, #1238, #991, .T. ) ;
#197=CARTESIAN_POINT ( 'NONE',  ( -0.03125000000000000000, -0.03125000000000000000, -0.1162848326531996102 ) ) ;
#211=DIRECTION ( 'NONE',  ( 0.000000000000000000, 1.000000000000000000, -0.000000000000000000 ) ) ;
#239=ORIENTED_EDGE ( 'NONE', *, *, #131, .T. ) ;
#303=AXIS2_PLACEMENT_3D ( 'NONE', #6878, #2039, #2570 ) ;
#328=EDGE_CURVE ( 'NONE', #7642, #4233, #2164, .T. ) ;
#382=EDGE_CURVE ( 'NONE', #5139, #1428, #6660, .T. ) ;
#410=CIRCLE ( 'NONE', #5003, 0.1150000000000000050 ) ;
#421=EDGE_CURVE ( 'NONE', #5293, #7642, #2198, .T. ) ;
#431=MECHANICAL_CONTEXT ( 'NONE', #5574, 'mechanical' ) ;
#457=PLANE ( 'NONE',  #1081 ) ;
#468=ORIENTED_EDGE ( 'NONE', *, *, #523, .T. ) ;
#476=DIRECTION ( 'NONE',  ( 0.000000000000000000, -1.000000000000000000, 0.000000000000000000 ) ) ;
#497=ORIENTED_EDGE ( 'NONE', *, *, #4721, .F. ) ;
#505=ORIENTED_EDGE ( 'NONE', *, *, #4721, .T. ) ;
#523=EDGE_CURVE ( 'NONE', #4775, #2638, #5633, .T. ) ;
#527=CARTESIAN_POINT ( 'NONE',  ( 0.03125000000000000000, 0.000000000000000000, -0.1162848326531996102 ) ) ;
#572=FACE_OUTER_BOUND ( 'NONE', #1266, .T. ) ;
#590=DIRECTION ( 'NONE',  ( -0.000000000000000000, -1.000000000000000000, -0.000000000000000000 ) ) ;
#618=CARTESIAN_POINT ( 'NONE',  ( 0.000000000000000000, 0.6350000000000000089, 0.000000000000000000 ) ) ;
#624=CARTESIAN_POINT ( 'NONE',  ( -0.03125000000000000000, 0.03124999999999997571, -0.1106726592253027830 ) ) ;
#643=DIRECTION ( 'NONE',  ( 0.000000000000000000, 0.000000000000000000, 1.000000000000000000 ) ) ;
#668=VERTEX_POINT ( 'NONE', #709 ) ;
#704=DIRECTION ( 'NONE',  ( 0.000000000000000000, -0.000000000000000000, -1.000000000000000000 ) ) ;
#709=CARTESIAN_POINT ( 'NONE',  ( 0.03125000000000000000, 0.03124999999999997571, -0.1106726592253027830 ) ) ;
#719=EDGE_CURVE ( 'NONE', #3809, #2089, #1377, .T. ) ;
#722=DIRECTION ( 'NONE',  ( 0.000000000000000000, 0.000000000000000000, 1.000000000000000000 ) ) ;
#740=DIRECTION ( 'NONE',  ( 0.000000000000000000, 0.000000000000000000, -1.000000000000000000 ) ) ;
#746=DIRECTION ( 'NONE',  ( -0.000000000000000000, -1.000000000000000000, -0.000000000000000000 ) ) ;
#755=DIRECTION ( 'NONE',  ( 0.000000000000000000, 0.000000000000000000, 1.000000000000000000 ) ) ;
#766=DIRECTION ( 'NONE',  ( 0.000000000000000000, 0.000000000000000000, -1.000000000000000000 ) ) ;
#801=LINE ( 'NONE', #2686, #4540 ) ;
#819=LINE ( 'NONE', #5823, #4777 ) ;
#839=ORIENTED_EDGE ( 'NONE', *, *, #6424, .T. ) ;
#846=VERTEX_POINT ( 'NONE', #2141 ) ;
#865=ORIENTED_EDGE ( 'NONE', *, *, #328, .T. ) ;
#869=MANIFOLD_SOLID_BREP ( 'Cut-Extrude1', #4398 ) ;
#892=CARTESIAN_POINT ( 'NONE',  ( -0.03125000000000000000, 0.000000000000000000, 0.000000000000000000 ) ) ;
#904=DESIGN_CONTEXT ( 'detailed design', #4059, 'design' ) ;
#905=ORIENTED_EDGE ( 'NONE', *, *, #382, .T. ) ;
#932=ORIENTED_EDGE ( 'NONE', *, *, #1171, .F. ) ;
#943=ORIENTED_EDGE ( 'NONE', *, *, #382, .F. ) ;
#946=ADVANCED_FACE ( 'NONE', ( #4848 ), #3569, .T. ) ;
#965=ORIENTED_EDGE ( 'NONE', *, *, #1887, .T. ) ;
#971=ORIENTED_EDGE ( 'NONE', *, *, #3093, .F. ) ;
#975=UNCERTAINTY_MEASURE_WITH_UNIT (LENGTH_MEASURE( 1.000000000000000082E-05 ), #4074, 'distance_accuracy_value', 'NONE');
#991=CIRCLE ( 'NONE', #7523, 0.1150000000000000050 ) ;
#992=CIRCLE ( 'NONE', #5438, 0.1204106507132265275 ) ;
#997=VECTOR ( 'NONE', #1776, 39.37007874015748143 ) ;
#1014=DIRECTION ( 'NONE',  ( 1.000000000000000000, 0.000000000000000000, 0.000000000000000000 ) ) ;
#1052=CYLINDRICAL_SURFACE ( 'NONE', #5340, 0.1150000000000000050 ) ;
#1081=AXIS2_PLACEMENT_3D ( 'NONE', #2958, #6320, #704 ) ;
#1163=ORIENTED_EDGE ( 'NONE', *, *, #421, .T. ) ;
#1165=CARTESIAN_POINT ( 'NONE',  ( 0.000000000000000000, -0.03125000000000000000, 0.000000000000000000 ) ) ;
#1171=EDGE_CURVE ( 'NONE', #1380, #1544, #3126, .T. ) ;
#1180=ADVANCED_FACE ( 'NONE', ( #5663 ), #3160, .T. ) ;
#1238=VERTEX_POINT ( 'NONE', #2783 ) ;
#1266=EDGE_LOOP ( 'NONE', ( #6103, #6463, #8052, #5215 ) ) ;
#1377=CIRCLE ( 'NONE', #3614, 0.1150000000000000050 ) ;
#1380=VERTEX_POINT ( 'NONE', #2286 ) ;
#1382=LINE ( 'NONE', #1927, #3094 ) ;
#1427=CARTESIAN_POINT ( 'NONE',  ( -0.03125000000000000000, -0.03125000000000000000, 0.000000000000000000 ) ) ;
#1428=VERTEX_POINT ( 'NONE', #5449 ) ;
#1434=CARTESIAN_POINT ( 'NONE',  ( 1.408343819019455843E-17, 0.03124999999999997571, 0.1150000000000000050 ) ) ;
#1444=DIRECTION ( 'NONE',  ( 0.000000000000000000, -1.000000000000000000, 0.000000000000000000 ) ) ;
#1513=CARTESIAN_POINT ( 'NONE',  ( -0.03125000000000000000, 0.03125000000000000000, -0.1204106507132265275 ) ) ;
#1544=VERTEX_POINT ( 'NONE', #5616 ) ;
#1612=DIRECTION ( 'NONE',  ( -0.000000000000000000, -1.000000000000000000, -0.000000000000000000 ) ) ;
#1660=CARTESIAN_POINT ( 'NONE',  ( 0.000000000000000000, 0.7500000000000001110, 0.000000000000000000 ) ) ;
#1667=ORIENTED_EDGE ( 'NONE', *, *, #2926, .F. ) ;
#1751=DIRECTION ( 'NONE',  ( 0.000000000000000000, 0.000000000000000000, 1.000000000000000000 ) ) ;
#1759=CIRCLE ( 'NONE', #7264, 0.1150000000000000050 ) ;
#1770=ORIENTED_EDGE ( 'NONE', *, *, #5789, .F. ) ;
#1776=DIRECTION ( 'NONE',  ( -0.000000000000000000, 1.000000000000000000, -0.000000000000000000 ) ) ;
#1812=ORIENTED_EDGE ( 'NONE', *, *, #8086, .F. ) ;
#1832=CARTESIAN_POINT ( 'NONE',  ( 0.03125000000000000000, -0.03125000000000000000, -0.1162848326531996102 ) ) ;
#1842=DIRECTION ( 'NONE',  ( 0.000000000000000000, 0.000000000000000000, -1.000000000000000000 ) ) ;
#1854=AXIS2_PLACEMENT_3D ( 'NONE', #3869, #5639, #7596 ) ;
#1887=EDGE_CURVE ( 'NONE', #4149, #5293, #410, .T. ) ;
#1927=CARTESIAN_POINT ( 'NONE',  ( -0.03125000000000000000, 0.7500000000000001110, 0.1106726592253027691 ) ) ;
#1956=ORIENTED_EDGE ( 'NONE', *, *, #6337, .F. ) ;
#1958=CARTESIAN_POINT ( 'NONE',  ( 0.000000000000000000, 0.03124999999999997571, 0.000000000000000000 ) ) ;
#1963=CARTESIAN_POINT ( 'NONE',  ( 0.000000000000000000, 0.7500000000000001110, 0.000000000000000000 ) ) ;
#2002=ORIENTED_EDGE ( 'NONE', *, *, #328, .F. ) ;
#2031=VECTOR ( 'NONE', #5390, 39.37007874015748143 ) ;
#2039=DIRECTION ( 'NONE',  ( -1.000000000000000000, 0.000000000000000000, 0.000000000000000000 ) ) ;
#2064=CIRCLE ( 'NONE', #4425, 0.1204106507132265275 ) ;
#2073=EDGE_LOOP ( 'NONE', ( #3074, #5073 ) ) ;
#2089=VERTEX_POINT ( 'NONE', #624 ) ;
#2141=CARTESIAN_POINT ( 'NONE',  ( -0.03125000000000000000, 0.03124999999999997571, 0.1106726592253027830 ) ) ;
#2164=CIRCLE ( 'NONE', #6742, 0.1150000000000000050 ) ;
#2165=CIRCLE ( 'NONE', #3209, 0.1150000000000000050 ) ;
#2180=CARTESIAN_POINT ( 'NONE',  ( 0.03125000000000000000, 0.03124999999999997571, 0.1106726592253027830 ) ) ;
#2191=VECTOR ( 'NONE', #7075, 39.37007874015748143 ) ;
#2198=LINE ( 'NONE', #7912, #7139 ) ;
#2199=ORIENTED_EDGE ( 'NONE', *, *, #4483, .T. ) ;
#2238=ADVANCED_FACE ( 'NONE', ( #572 ), #457, .F. ) ;
#2242=LINE ( 'NONE', #6559, #5541 ) ;
#2272=CARTESIAN_POINT ( 'NONE',  ( 0.03125000000000000000, 0.000000000000000000, 0.000000000000000000 ) ) ;
#2286=CARTESIAN_POINT ( 'NONE',  ( -0.03125000000000000000, -0.03125000000000000000, 0.1162848326531996240 ) ) ;
#2305=ORIENTED_EDGE ( 'NONE', *, *, #719, .T. ) ;
#2353=CARTESIAN_POINT ( 'NONE',  ( 0.03125000000000000000, 0.03125000000000000000, -0.1204106507132265275 ) ) ;
#2367=ORIENTED_EDGE ( 'NONE', *, *, #4246, .T. ) ;
#2379=CARTESIAN_POINT ( 'NONE',  ( 0.000000000000000000, -0.03125000000000000000, 0.000000000000000000 ) ) ;
#2418=LINE ( 'NONE', #7314, #6329 ) ;
#2452=DIRECTION ( 'NONE',  ( 0.000000000000000000, 1.000000000000000000, -0.000000000000000000 ) ) ;
#2469=ORIENTED_EDGE ( 'NONE', *, *, #421, .F. ) ;
#2477=DIRECTION ( 'NONE',  ( -0.000000000000000000, -1.000000000000000000, -0.000000000000000000 ) ) ;
#2493=DIRECTION ( 'NONE',  ( -0.000000000000000000, -1.000000000000000000, -0.000000000000000000 ) ) ;
#2530=DIMENSIONAL_EXPONENTS ( 1.000000000000000000, 0.000000000000000000, 0.000000000000000000, 0.000000000000000000, 0.000000000000000000, 0.000000000000000000, 0.000000000000000000 ) ;
#2534=VECTOR ( 'NONE', #3549, 39.37007874015748143 ) ;
#2570=DIRECTION ( 'NONE',  ( 0.000000000000000000, 0.000000000000000000, 1.000000000000000000 ) ) ;
#2592=LINE ( 'NONE', #7064, #3985 ) ;
#2601=FACE_OUTER_BOUND ( 'NONE', #6415, .T. ) ;
#2632=ORIENTED_EDGE ( 'NONE', *, *, #3093, .T. ) ;
#2638=VERTEX_POINT ( 'NONE', #527 ) ;
#2675=DIRECTION ( 'NONE',  ( 0.000000000000000000, 0.000000000000000000, 1.000000000000000000 ) ) ;
#2686=CARTESIAN_POINT ( 'NONE',  ( -0.03125000000000000000, 0.03125000000000000000, -0.1204106507132265275 ) ) ;
#2701=ORIENTED_EDGE ( 'NONE', *, *, #8086, .T. ) ;
#2704=AXIS2_PLACEMENT_3D ( 'NONE', #1165, #7319, #3051 ) ;
#2722=EDGE_LOOP ( 'NONE', ( #1770, #905, #839, #6019 ) ) ;
#2729=CARTESIAN_POINT ( 'NONE',  ( 0.000000000000000000, -0.03125000000000000000, 0.000000000000000000 ) ) ;
#2771=( GEOMETRIC_REPRESENTATION_CONTEXT ( 3 ) GLOBAL_UNCERTAINTY_ASSIGNED_CONTEXT ( ( #975 ) ) GLOBAL_UNIT_ASSIGNED_CONTEXT ( ( #4074, #4653, #3502 ) ) REPRESENTATION_CONTEXT ( 'NONE', 'WORKASPACE' ) );
#2783=CARTESIAN_POINT ( 'NONE',  ( 0.03125000000000000000, 0.000000000000000000, 0.1106726592253027830 ) ) ;
#2827=VERTEX_POINT ( 'NONE', #7651 ) ;
#2831=ADVANCED_FACE ( 'NONE', ( #2601 ), #4431, .F. ) ;
#2910=CARTESIAN_POINT ( 'NONE',  ( 0.000000000000000000, -0.03125000000000000000, 0.000000000000000000 ) ) ;
#2926=EDGE_CURVE ( 'NONE', #2089, #4761, #2242, .T. ) ;
#2958=CARTESIAN_POINT ( 'NONE',  ( 0.000000000000000000, 0.000000000000000000, 0.000000000000000000 ) ) ;
#3051=DIRECTION ( 'NONE',  ( 0.000000000000000000, -0.000000000000000000, -1.000000000000000000 ) ) ;
#3074=ORIENTED_EDGE ( 'NONE', *, *, #1887, .F. ) ;
#3093=EDGE_CURVE ( 'NONE', #3518, #2827, #3644, .T. ) ;
#3094=VECTOR ( 'NONE', #5208, 39.37007874015748143 ) ;
#3122=CARTESIAN_POINT ( 'NONE',  ( 0.000000000000000000, 0.000000000000000000, 0.000000000000000000 ) ) ;
#3126=LINE ( 'NONE', #1427, #4797 ) ;
#3129=ORIENTED_EDGE ( 'NONE', *, *, #4090, .T. ) ;
#3145=EDGE_LOOP ( 'NONE', ( #8004, #3874, #505, #971, #4106, #3253, #8087, #7722 ) ) ;
#3160=CYLINDRICAL_SURFACE ( 'NONE', #4411, 0.1150000000000000050 ) ;
#3174=CARTESIAN_POINT ( 'NONE',  ( 1.408343819019455843E-17, 0.6350000000000000089, 0.1150000000000000050 ) ) ;
#3209=AXIS2_PLACEMENT_3D ( 'NONE', #1958, #2452, #3813 ) ;
#3227=VECTOR ( 'NONE', #4217, 39.37007874015748143 ) ;
#3253=ORIENTED_EDGE ( 'NONE', *, *, #3285, .F. ) ;
#3273=VERTEX_POINT ( 'NONE', #5880 ) ;
#3275=DIRECTION ( 'NONE',  ( 0.000000000000000000, 0.000000000000000000, -1.000000000000000000 ) ) ;
#3285=EDGE_CURVE ( 'NONE', #4233, #1238, #7154, .T. ) ;
#3303=CARTESIAN_POINT ( 'NONE',  ( 0.000000000000000000, 0.03124999999999997571, -0.1150000000000000050 ) ) ;
#3345=ORIENTED_EDGE ( 'NONE', *, *, #6198, .T. ) ;
#3381=EDGE_CURVE ( 'NONE', #4761, #3273, #2418, .T. ) ;
#3492=EDGE_CURVE ( 'NONE', #4775, #2827, #7515, .T. ) ;
#3496=PRODUCT_DEFINITION_SHAPE ( 'NONE', 'NONE',  #7247 ) ;
#3502=( NAMED_UNIT ( * ) SI_UNIT ( $, .STERADIAN. ) SOLID_ANGLE_UNIT ( ) );
#3518=VERTEX_POINT ( 'NONE', #7669 ) ;
#3549=DIRECTION ( 'NONE',  ( 0.000000000000000000, -1.000000000000000000, 0.000000000000000000 ) ) ;
#3555=AXIS2_PLACEMENT_3D ( 'NONE', #5720, #6981, #135 ) ;
#3569=CYLINDRICAL_SURFACE ( 'NONE', #4922, 0.1204106507132265275 ) ;
#3614=AXIS2_PLACEMENT_3D ( 'NONE', #97, #211, #7511 ) ;
#3644=LINE ( 'NONE', #6059, #2534 ) ;
#3659=FACE_OUTER_BOUND ( 'NONE', #2073, .T. ) ;
#3715=CARTESIAN_POINT ( 'NONE',  ( -0.03125000000000000000, 0.000000000000000000, 0.1162848326531996102 ) ) ;
#3770=DIRECTION ( 'NONE',  ( -0.000000000000000000, -0.000000000000000000, -1.000000000000000000 ) ) ;
#3794=ADVANCED_FACE ( 'NONE', ( #6953 ), #6462, .T. ) ;
#3809=VERTEX_POINT ( 'NONE', #3303 ) ;
#3813=DIRECTION ( 'NONE',  ( 0.000000000000000000, 0.000000000000000000, 1.000000000000000000 ) ) ;
#3840=DIRECTION ( 'NONE',  ( -0.000000000000000000, 1.000000000000000000, -0.000000000000000000 ) ) ;
#3869=CARTESIAN_POINT ( 'NONE',  ( 0.000000000000000000, -0.03125000000000000000, 0.000000000000000000 ) ) ;
#3874=ORIENTED_EDGE ( 'NONE', *, *, #523, .F. ) ;
#3888=CIRCLE ( 'NONE', #92, 0.1150000000000000050 ) ;
#3892=EDGE_LOOP ( 'NONE', ( #932, #2701 ) ) ;
#3894=ADVANCED_FACE ( 'NONE', ( #4123 ), #5321, .F. ) ;
#3899=AXIS2_PLACEMENT_3D ( 'NONE', #6727, #1444, #6031 ) ;
#3967=ORIENTED_EDGE ( 'NONE', *, *, #3492, .T. ) ;
#3979=CARTESIAN_POINT ( 'NONE',  ( 0.000000000000000000, -0.03125000000000000000, 0.000000000000000000 ) ) ;
#3985=VECTOR ( 'NONE', #4565, 39.37007874015748143 ) ;
#4028=FACE_OUTER_BOUND ( 'NONE', #6182, .T. ) ;
#4043=DIRECTION ( 'NONE',  ( -0.000000000000000000, -1.000000000000000000, -0.000000000000000000 ) ) ;
#4055=CARTESIAN_POINT ( 'NONE',  ( 0.03125000000000000000, 0.000000000000000000, -0.1106726592253027830 ) ) ;
#4059=APPLICATION_CONTEXT ( 'configuration controlled 3d designs of mechanical parts and assemblies' ) ;
#4074=( CONVERSION_BASED_UNIT ( 'INCH', #7152 ) LENGTH_UNIT ( ) NAMED_UNIT ( #2530 ) );
#4088=DIRECTION ( 'NONE',  ( -0.000000000000000000, -1.000000000000000000, -0.000000000000000000 ) ) ;
#4090=EDGE_CURVE ( 'NONE', #5293, #4149, #1759, .T. ) ;
#4100=ORIENTED_EDGE ( 'NONE', *, *, #6198, .F. ) ;
#4106=ORIENTED_EDGE ( 'NONE', *, *, #5298, .F. ) ;
#4123=FACE_OUTER_BOUND ( 'NONE', #3145, .T. ) ;
#4149=VERTEX_POINT ( 'NONE', #6909 ) ;
#4169=DIRECTION ( 'NONE',  ( -0.000000000000000000, -1.000000000000000000, -0.000000000000000000 ) ) ;
#4184=DIRECTION ( 'NONE',  ( 0.000000000000000000, -1.000000000000000000, 0.000000000000000000 ) ) ;
#4217=DIRECTION ( 'NONE',  ( -0.000000000000000000, 1.000000000000000000, -0.000000000000000000 ) ) ;
#4233=VERTEX_POINT ( 'NONE', #2180 ) ;
#4246=EDGE_CURVE ( 'NONE', #5062, #668, #819, .T. ) ;
#4274=DIRECTION ( 'NONE',  ( 0.000000000000000000, 1.000000000000000000, 0.000000000000000000 ) ) ;
#4330=ADVANCED_FACE ( 'NONE', ( #7787 ), #4678, .T. ) ;
#4380=LINE ( 'NONE', #5485, #3227 ) ;
#4385=ORIENTED_EDGE ( 'NONE', *, *, #7980, .T. ) ;
#4398=CLOSED_SHELL ( 'NONE', ( #6747, #6991, #946, #4330, #1180, #7189, #2238, #3794, #7884, #7444, #2831, #3894 ) ) ;
#4411=AXIS2_PLACEMENT_3D ( 'NONE', #1963, #2493, #740 ) ;
#4425=AXIS2_PLACEMENT_3D ( 'NONE', #3122, #5621, #1842 ) ;
#4431=PLANE ( 'NONE',  #303 ) ;
#4444=EDGE_CURVE ( 'NONE', #2638, #3518, #992, .T. ) ;
#4467=EDGE_LOOP ( 'NONE', ( #965, #1163, #865, #5161, #6406, #2367, #4385, #6678 ) ) ;
#4483=EDGE_CURVE ( 'NONE', #846, #7642, #2165, .T. ) ;
#4539=ORIENTED_EDGE ( 'NONE', *, *, #4483, .F. ) ;
#4540=VECTOR ( 'NONE', #3770, 39.37007874015748143 ) ;
#4565=DIRECTION ( 'NONE',  ( 0.000000000000000000, 0.000000000000000000, 1.000000000000000000 ) ) ;
#4585=DIRECTION ( 'NONE',  ( 0.000000000000000000, -1.000000000000000000, 0.000000000000000000 ) ) ;
#4653=( NAMED_UNIT ( * ) PLANE_ANGLE_UNIT ( ) SI_UNIT ( $, .RADIAN. ) );
#4672=PLANE ( 'NONE',  #6117 ) ;
#4678=PLANE ( 'NONE',  #5165 ) ;
#4721=EDGE_CURVE ( 'NONE', #4775, #2827, #4870, .T. ) ;
#4741=ORIENTED_EDGE ( 'NONE', *, *, #5789, .T. ) ;
#4761=VERTEX_POINT ( 'NONE', #6919 ) ;
#4775=VERTEX_POINT ( 'NONE', #1832 ) ;
#4777=VECTOR ( 'NONE', #6435, 39.37007874015748143 ) ;
#4780=SHAPE_DEFINITION_REPRESENTATION ( #3496, #6436 ) ;
#4784=VECTOR ( 'NONE', #1751, 39.37007874015748143 ) ;
#4797=VECTOR ( 'NONE', #3275, 39.37007874015748143 ) ;
#4847=FACE_OUTER_BOUND ( 'NONE', #2722, .T. ) ;
#4848=FACE_OUTER_BOUND ( 'NONE', #5701, .T. ) ;
#4865=CARTESIAN_POINT ( 'NONE',  ( 0.000000000000000000, 0.000000000000000000, 0.000000000000000000 ) ) ;
#4870=LINE ( 'NONE', #7367, #4784 ) ;
#4893=DIRECTION ( 'NONE',  ( 0.000000000000000000, -1.000000000000000000, 0.000000000000000000 ) ) ;
#4922=AXIS2_PLACEMENT_3D ( 'NONE', #2910, #8021, #4967 ) ;
#4937=CARTESIAN_POINT ( 'NONE',  ( 0.03125000000000000000, -0.03125000000000000000, -0.1162848326531996102 ) ) ;
#4967=DIRECTION ( 'NONE',  ( 0.000000000000000000, 0.000000000000000000, 1.000000000000000000 ) ) ;
#5003=AXIS2_PLACEMENT_3D ( 'NONE', #6825, #2477, #5784 ) ;
#5040=DIRECTION ( 'NONE',  ( 0.000000000000000000, -1.000000000000000000, 0.000000000000000000 ) ) ;
#5049=ORIENTED_EDGE ( 'NONE', *, *, #5896, .F. ) ;
#5062=VERTEX_POINT ( 'NONE', #4055 ) ;
#5066=DIRECTION ( 'NONE',  ( 0.000000000000000000, 1.000000000000000000, -0.000000000000000000 ) ) ;
#5069=CIRCLE ( 'NONE', #6123, 0.1150000000000000050 ) ;
#5073=ORIENTED_EDGE ( 'NONE', *, *, #4090, .F. ) ;
#5139=VERTEX_POINT ( 'NONE', #3715 ) ;
#5150=VECTOR ( 'NONE', #4043, 39.37007874015748143 ) ;
#5154=AXIS2_PLACEMENT_3D ( 'NONE', #2379, #4893, #7389 ) ;
#5158=LINE ( 'NONE', #197, #8035 ) ;
#5161=ORIENTED_EDGE ( 'NONE', *, *, #3285, .T. ) ;
#5165=AXIS2_PLACEMENT_3D ( 'NONE', #3979, #4184, #5994 ) ;
#5208=DIRECTION ( 'NONE',  ( 0.000000000000000000, 1.000000000000000000, 0.000000000000000000 ) ) ;
#5215=ORIENTED_EDGE ( 'NONE', *, *, #5298, .T. ) ;
#5278=EDGE_LOOP ( 'NONE', ( #497, #3967 ) ) ;
#5293=VERTEX_POINT ( 'NONE', #3174 ) ;
#5298=EDGE_CURVE ( 'NONE', #1238, #3518, #2592, .T. ) ;
#5321=PLANE ( 'NONE',  #49 ) ;
#5336=ADVANCED_BREP_SHAPE_REPRESENTATION ( '', ( #869, #3555 ), #2771 ) ;
#5340=AXIS2_PLACEMENT_3D ( 'NONE', #1660, #4169, #6664 ) ;
#5355=( LENGTH_UNIT ( ) NAMED_UNIT ( * ) SI_UNIT ( $, .METRE. ) );
#5390=DIRECTION ( 'NONE',  ( 0.000000000000000000, 0.000000000000000000, -1.000000000000000000 ) ) ;
#5392=CIRCLE ( 'NONE', #1854, 0.1204106507132265275 ) ;
#5397=LINE ( 'NONE', #2272, #2191 ) ;
#5431=DIRECTION ( 'NONE',  ( 0.000000000000000000, 0.000000000000000000, -1.000000000000000000 ) ) ;
#5438=AXIS2_PLACEMENT_3D ( 'NONE', #5531, #5040, #5702 ) ;
#5449=CARTESIAN_POINT ( 'NONE',  ( -0.03125000000000000000, 0.000000000000000000, 0.1106726592253027830 ) ) ;
#5485=CARTESIAN_POINT ( 'NONE',  ( -0.03125000000000000000, -0.03125000000000000000, 0.1162848326531996102 ) ) ;
#5505=ORIENTED_EDGE ( 'NONE', *, *, #7980, .F. ) ;
#5531=CARTESIAN_POINT ( 'NONE',  ( 0.000000000000000000, 0.000000000000000000, 0.000000000000000000 ) ) ;
#5541=VECTOR ( 'NONE', #4088, 39.37007874015748143 ) ;
#5553=AXIS2_PLACEMENT_3D ( 'NONE', #2729, #3840, #722 ) ;
#5574=APPLICATION_CONTEXT ( 'configuration controlled 3d designs of mechanical parts and assemblies' ) ;
#5604=FACE_OUTER_BOUND ( 'NONE', #5278, .T. ) ;
#5616=CARTESIAN_POINT ( 'NONE',  ( -0.03125000000000000000, -0.03125000000000000000, -0.1162848326531996102 ) ) ;
#5621=DIRECTION ( 'NONE',  ( 0.000000000000000000, -1.000000000000000000, 0.000000000000000000 ) ) ;
#5633=LINE ( 'NONE', #4937, #997 ) ;
#5639=DIRECTION ( 'NONE',  ( 0.000000000000000000, -1.000000000000000000, 0.000000000000000000 ) ) ;
#5663=FACE_OUTER_BOUND ( 'NONE', #5774, .T. ) ;
#5701=EDGE_LOOP ( 'NONE', ( #1812, #3345, #4741, #6612 ) ) ;
#5702=DIRECTION ( 'NONE',  ( 0.000000000000000000, 0.000000000000000000, -1.000000000000000000 ) ) ;
#5720=CARTESIAN_POINT ( 'NONE',  ( 0.000000000000000000, 0.000000000000000000, 0.000000000000000000 ) ) ;
#5774=EDGE_LOOP ( 'NONE', ( #2469, #3129, #7751, #2305, #6133, #99, #6004, #2199 ) ) ;
#5784=DIRECTION ( 'NONE',  ( 0.000000000000000000, 0.000000000000000000, -1.000000000000000000 ) ) ;
#5789=EDGE_CURVE ( 'NONE', #5139, #3273, #2064, .T. ) ;
#5823=CARTESIAN_POINT ( 'NONE',  ( 0.03125000000000000000, 0.7500000000000001110, -0.1106726592253027691 ) ) ;
#5880=CARTESIAN_POINT ( 'NONE',  ( -0.03125000000000000000, 0.000000000000000000, -0.1162848326531996102 ) ) ;
#5896=EDGE_CURVE ( 'NONE', #1428, #846, #1382, .T. ) ;
#5908=DIRECTION ( 'NONE',  ( 0.000000000000000000, 0.000000000000000000, 1.000000000000000000 ) ) ;
#5925=PRODUCT_DEFINITION_FORMATION_WITH_SPECIFIED_SOURCE ( 'ANY', '', #7217, .NOT_KNOWN. ) ;
#5994=DIRECTION ( 'NONE',  ( 0.000000000000000000, -0.000000000000000000, -1.000000000000000000 ) ) ;
#6004=ORIENTED_EDGE ( 'NONE', *, *, #5896, .T. ) ;
#6019=ORIENTED_EDGE ( 'NONE', *, *, #3381, .T. ) ;
#6031=DIRECTION ( 'NONE',  ( 0.000000000000000000, -0.000000000000000000, -1.000000000000000000 ) ) ;
#6059=CARTESIAN_POINT ( 'NONE',  ( 0.03125000000000000000, -0.03125000000000000000, 0.1162848326531996102 ) ) ;
#6103=ORIENTED_EDGE ( 'NONE', *, *, #4444, .F. ) ;
#6117=AXIS2_PLACEMENT_3D ( 'NONE', #1513, #6530, #5908 ) ;
#6123=AXIS2_PLACEMENT_3D ( 'NONE', #7562, #7628, #755 ) ;
#6133=ORIENTED_EDGE ( 'NONE', *, *, #2926, .T. ) ;
#6182=EDGE_LOOP ( 'NONE', ( #239, #2002, #4539, #7951, #6769, #5505 ) ) ;
#6198=EDGE_CURVE ( 'NONE', #1380, #5139, #4380, .T. ) ;
#6243=SPHERICAL_SURFACE ( 'NONE', #7691, 0.1150000000000000050 ) ;
#6317=ORIENTED_EDGE ( 'NONE', *, *, #1171, .T. ) ;
#6320=DIRECTION ( 'NONE',  ( 0.000000000000000000, -1.000000000000000000, 0.000000000000000000 ) ) ;
#6329=VECTOR ( 'NONE', #6814, 39.37007874015748143 ) ;
#6337=EDGE_CURVE ( 'NONE', #846, #2089, #801, .T. ) ;
#6361=LINE ( 'NONE', #7621, #6634 ) ;
#6383=DIRECTION ( 'NONE',  ( 0.000000000000000000, -1.000000000000000000, 0.000000000000000000 ) ) ;
#6406=ORIENTED_EDGE ( 'NONE', *, *, #168, .F. ) ;
#6415=EDGE_LOOP ( 'NONE', ( #943, #4100, #6317, #7626, #6498, #1667, #1956, #5049 ) ) ;
#6424=EDGE_CURVE ( 'NONE', #1428, #4761, #3888, .T. ) ;
#6435=DIRECTION ( 'NONE',  ( 0.000000000000000000, 1.000000000000000000, 0.000000000000000000 ) ) ;
#6436=SHAPE_REPRESENTATION ( 'Cleco, Fastener, Pusher', ( #3555 ), #2771 ) ;
#6462=CYLINDRICAL_SURFACE ( 'NONE', #5553, 0.1204106507132265275 ) ;
#6463=ORIENTED_EDGE ( 'NONE', *, *, #6595, .T. ) ;
#6498=ORIENTED_EDGE ( 'NONE', *, *, #3381, .F. ) ;
#6530=DIRECTION ( 'NONE',  ( 0.000000000000000000, 1.000000000000000000, -0.000000000000000000 ) ) ;
#6537=EDGE_LOOP ( 'NONE', ( #6744, #468, #12, #2632 ) ) ;
#6559=CARTESIAN_POINT ( 'NONE',  ( -0.03125000000000000000, 0.7500000000000001110, -0.1106726592253027691 ) ) ;
#6577=CARTESIAN_POINT ( 'NONE',  ( 0.03125000000000000000, 0.7500000000000001110, 0.1106726592253027691 ) ) ;
#6595=EDGE_CURVE ( 'NONE', #2638, #5062, #5397, .T. ) ;
#6612=ORIENTED_EDGE ( 'NONE', *, *, #29, .T. ) ;
#6623=CARTESIAN_POINT ( 'NONE',  ( 0.03125000000000000000, 0.03125000000000000000, -0.1204106507132265275 ) ) ;
#6634=VECTOR ( 'NONE', #746, 39.37007874015748143 ) ;
#6660=LINE ( 'NONE', #892, #2031 ) ;
#6664=DIRECTION ( 'NONE',  ( 0.000000000000000000, 0.000000000000000000, -1.000000000000000000 ) ) ;
#6678=ORIENTED_EDGE ( 'NONE', *, *, #7688, .F. ) ;
#6727=CARTESIAN_POINT ( 'NONE',  ( 0.000000000000000000, 0.000000000000000000, 0.000000000000000000 ) ) ;
#6742=AXIS2_PLACEMENT_3D ( 'NONE', #6986, #5066, #2675 ) ;
#6744=ORIENTED_EDGE ( 'NONE', *, *, #3492, .F. ) ;
#6747=ADVANCED_FACE ( 'NONE', ( #7322 ), #1052, .T. ) ;
#6769=ORIENTED_EDGE ( 'NONE', *, *, #719, .F. ) ;
#6783=CARTESIAN_POINT ( 'NONE',  ( 0.000000000000000000, 0.6350000000000000089, 0.000000000000000000 ) ) ;
#6788=LINE ( 'NONE', #2353, #7004 ) ;
#6814=DIRECTION ( 'NONE',  ( 0.000000000000000000, 0.000000000000000000, -1.000000000000000000 ) ) ;
#6818=DIRECTION ( 'NONE',  ( 0.000000000000000000, 0.000000000000000000, -1.000000000000000000 ) ) ;
#6825=CARTESIAN_POINT ( 'NONE',  ( 0.000000000000000000, 0.6350000000000000089, 0.000000000000000000 ) ) ;
#6878=CARTESIAN_POINT ( 'NONE',  ( -0.03125000000000000000, 0.03125000000000000000, -0.1204106507132265275 ) ) ;
#6909=CARTESIAN_POINT ( 'NONE',  ( 0.000000000000000000, 0.6350000000000000089, -0.1150000000000000050 ) ) ;
#6919=CARTESIAN_POINT ( 'NONE',  ( -0.03125000000000000000, 0.000000000000000000, -0.1106726592253027830 ) ) ;
#6953=FACE_OUTER_BOUND ( 'NONE', #6537, .T. ) ;
#6981=DIRECTION ( 'NONE',  ( 0.000000000000000000, 0.000000000000000000, 1.000000000000000000 ) ) ;
#6986=CARTESIAN_POINT ( 'NONE',  ( 0.000000000000000000, 0.03124999999999997571, 0.000000000000000000 ) ) ;
#6991=ADVANCED_FACE ( 'NONE', ( #4847 ), #7260, .F. ) ;
#7004=VECTOR ( 'NONE', #643, 39.37007874015748143 ) ;
#7064=CARTESIAN_POINT ( 'NONE',  ( 0.03125000000000000000, 0.000000000000000000, 0.000000000000000000 ) ) ;
#7075=DIRECTION ( 'NONE',  ( 0.000000000000000000, 0.000000000000000000, 1.000000000000000000 ) ) ;
#7139=VECTOR ( 'NONE', #1612, 39.37007874015748143 ) ;
#7152=LENGTH_MEASURE_WITH_UNIT ( LENGTH_MEASURE( 0.02539999999999999897 ), #5355 );
#7154=LINE ( 'NONE', #6577, #5150 ) ;
#7189=ADVANCED_FACE ( 'NONE', ( #3659 ), #6243, .T. ) ;
#7217=PRODUCT ( 'Cleco, Fastener, Pusher', 'Cleco, Fastener, Pusher', '', ( #431 ) ) ;
#7247=PRODUCT_DEFINITION ( 'UNKNOWN', '', #5925, #904 ) ;
#7260=PLANE ( 'NONE',  #3899 ) ;
#7264=AXIS2_PLACEMENT_3D ( 'NONE', #6783, #590, #6818 ) ;
#7314=CARTESIAN_POINT ( 'NONE',  ( -0.03125000000000000000, 0.000000000000000000, 0.000000000000000000 ) ) ;
#7319=DIRECTION ( 'NONE',  ( 0.000000000000000000, -1.000000000000000000, 0.000000000000000000 ) ) ;
#7322=FACE_OUTER_BOUND ( 'NONE', #4467, .T. ) ;
#7367=CARTESIAN_POINT ( 'NONE',  ( 0.03125000000000000000, -0.03125000000000000000, 0.000000000000000000 ) ) ;
#7389=DIRECTION ( 'NONE',  ( 0.000000000000000000, 0.000000000000000000, -1.000000000000000000 ) ) ;
#7444=ADVANCED_FACE ( 'NONE', ( #4028 ), #4672, .F. ) ;
#7474=PLANE ( 'NONE',  #2704 ) ;
#7511=DIRECTION ( 'NONE',  ( 0.000000000000000000, 0.000000000000000000, 1.000000000000000000 ) ) ;
#7515=CIRCLE ( 'NONE', #5154, 0.1204106507132265275 ) ;
#7523=AXIS2_PLACEMENT_3D ( 'NONE', #4865, #476, #18 ) ;
#7562=CARTESIAN_POINT ( 'NONE',  ( 0.000000000000000000, 0.03124999999999997571, 0.000000000000000000 ) ) ;
#7571=CARTESIAN_POINT ( 'NONE',  ( 0.000000000000000000, 0.000000000000000000, 0.000000000000000000 ) ) ;
#7596=DIRECTION ( 'NONE',  ( 0.000000000000000000, 0.000000000000000000, -1.000000000000000000 ) ) ;
#7621=CARTESIAN_POINT ( 'NONE',  ( 0.000000000000000000, 0.7500000000000001110, -0.1150000000000000050 ) ) ;
#7626=ORIENTED_EDGE ( 'NONE', *, *, #29, .F. ) ;
#7628=DIRECTION ( 'NONE',  ( 0.000000000000000000, 1.000000000000000000, -0.000000000000000000 ) ) ;
#7642=VERTEX_POINT ( 'NONE', #1434 ) ;
#7651=CARTESIAN_POINT ( 'NONE',  ( 0.03125000000000000000, -0.03125000000000000000, 0.1162848326531996240 ) ) ;
#7669=CARTESIAN_POINT ( 'NONE',  ( 0.03125000000000000000, 0.000000000000000000, 0.1162848326531996102 ) ) ;
#7688=EDGE_CURVE ( 'NONE', #4149, #3809, #6361, .T. ) ;
#7691=AXIS2_PLACEMENT_3D ( 'NONE', #618, #4274, #8020 ) ;
#7722=ORIENTED_EDGE ( 'NONE', *, *, #4246, .F. ) ;
#7751=ORIENTED_EDGE ( 'NONE', *, *, #7688, .T. ) ;
#7757=SHAPE_REPRESENTATION_RELATIONSHIP ( 'NONE' , 'NONE' ,  #6436, #5336 ) ;
#7787=FACE_OUTER_BOUND ( 'NONE', #3892, .T. ) ;
#7884=ADVANCED_FACE ( 'NONE', ( #5604 ), #7474, .T. ) ;
#7912=CARTESIAN_POINT ( 'NONE',  ( 1.408343819019455843E-17, 0.7500000000000001110, 0.1150000000000000050 ) ) ;
#7951=ORIENTED_EDGE ( 'NONE', *, *, #6337, .T. ) ;
#7980=EDGE_CURVE ( 'NONE', #668, #3809, #5069, .T. ) ;
#8004=ORIENTED_EDGE ( 'NONE', *, *, #6595, .F. ) ;
#8020=DIRECTION ( 'NONE',  ( 1.000000000000000000, 0.000000000000000000, 0.000000000000000000 ) ) ;
#8021=DIRECTION ( 'NONE',  ( -0.000000000000000000, 1.000000000000000000, -0.000000000000000000 ) ) ;
#8035=VECTOR ( 'NONE', #4585, 39.37007874015748143 ) ;
#8052=ORIENTED_EDGE ( 'NONE', *, *, #168, .T. ) ;
#8086=EDGE_CURVE ( 'NONE', #1380, #1544, #5392, .T. ) ;
#8087=ORIENTED_EDGE ( 'NONE', *, *, #131, .F. ) ;
#8101=COLOUR_RGB('Deep Blue', 0.66274510, 0.83137255, 0.94901961);
#8102=FILL_AREA_STYLE_COLOUR('',#8101);
#8103=FILL_AREA_STYLE('',(#8102));
#8104=SURFACE_STYLE_FILL_AREA(#8103);
#8105=SURFACE_SIDE_STYLE('',(#8104));
#8106=SURFACE_STYLE_USAGE(.BOTH.,#8105);
#8107=PRESENTATION_STYLE_ASSIGNMENT((#8106));
#8154=STYLED_ITEM('',(#8107),#869);
#8155=MECHANICAL_DESIGN_GEOMETRIC_PRESENTATION_REPRESENTATION('',(#8154),#2771);
ENDSEC;
END-ISO-10303-21;
